ISO-10303-21;
HEADER;
/* Generated by software containing ST-Developer
 * from STEP Tools, Inc. (www.steptools.com) 
 */

FILE_DESCRIPTION(
/* description */ ('Spring compression tester'),
/* implementation_level */ '2;1');

FILE_NAME(
/* name */ 'Socket Set Screw - M5x8.step',
/* time_stamp */ '2026-10-28T03:24:11-07:00',
/* author */ (''),
/* organization */ (''),
/* preprocessor_version */ 'ST-DEVELOPER v20.2',
/* originating_system */ 'Autodesk Translation Framework v15.17.0.0',
/* authorisation */ '');

FILE_SCHEMA (('AUTOMOTIVE_DESIGN { 1 0 10303 214 3 1 1 }'));
ENDSEC;

DATA;
#10=MECHANICAL_DESIGN_GEOMETRIC_PRESENTATION_REPRESENTATION('',(#1176),#43521);
#978=CONICAL_SURFACE('',#21140,0.235,0.785398163397448);
#979=CONICAL_SURFACE('',#21144,0.2125,0.785398163397448);
#1041=SHAPE_REPRESENTATION_RELATIONSHIP('SRR','None',#43858,#1101);
#1101=ADVANCED_BREP_SHAPE_REPRESENTATION('',(#1245),#43518);
#1176=STYLED_ITEM('',(#44209),#1245);
#1245=MANIFOLD_SOLID_BREP('Body1',#18619);
#1585=FACE_BOUND('',#4577,.T.);
#2148=PLANE('',#21131);
#2149=PLANE('',#21132);
#2150=PLANE('',#21133);
#2151=PLANE('',#21134);
#2152=PLANE('',#21135);
#2153=PLANE('',#21136);
#2154=PLANE('',#21137);
#2155=PLANE('',#21138);
#2156=PLANE('',#21146);
#3184=FACE_OUTER_BOUND('',#4569,.T.);
#3185=FACE_OUTER_BOUND('',#4570,.T.);
#3186=FACE_OUTER_BOUND('',#4571,.T.);
#3187=FACE_OUTER_BOUND('',#4572,.T.);
#3188=FACE_OUTER_BOUND('',#4573,.T.);
#3189=FACE_OUTER_BOUND('',#4574,.T.);
#3190=FACE_OUTER_BOUND('',#4575,.T.);
#3191=FACE_OUTER_BOUND('',#4576,.T.);
#3192=FACE_OUTER_BOUND('',#4578,.T.);
#3193=FACE_OUTER_BOUND('',#4579,.T.);
#3194=FACE_OUTER_BOUND('',#4580,.T.);
#3195=FACE_OUTER_BOUND('',#4581,.T.);
#4569=EDGE_LOOP('',(#16979,#16980,#16981,#16982));
#4570=EDGE_LOOP('',(#16983,#16984,#16985,#16986));
#4571=EDGE_LOOP('',(#16987,#16988,#16989,#16990));
#4572=EDGE_LOOP('',(#16991,#16992,#16993,#16994));
#4573=EDGE_LOOP('',(#16995,#16996,#16997,#16998));
#4574=EDGE_LOOP('',(#16999,#17000,#17001,#17002));
#4575=EDGE_LOOP('',(#17003,#17004,#17005,#17006,#17007,#17008));
#4576=EDGE_LOOP('',(#17009));
#4577=EDGE_LOOP('',(#17010,#17011,#17012,#17013,#17014,#17015));
#4578=EDGE_LOOP('',(#17016,#17017,#17018,#17019));
#4579=EDGE_LOOP('',(#17020,#17021,#17022,#17023));
#4580=EDGE_LOOP('',(#17024,#17025,#17026,#17027));
#4581=EDGE_LOOP('',(#17028));
#5991=LINE('',#43237,#7423);
#5992=LINE('',#43239,#7424);
#5993=LINE('',#43241,#7425);
#5994=LINE('',#43242,#7426);
#5995=LINE('',#43245,#7427);
#5996=LINE('',#43247,#7428);
#5997=LINE('',#43248,#7429);
#5998=LINE('',#43251,#7430);
#5999=LINE('',#43253,#7431);
#6000=LINE('',#43254,#7432);
#6001=LINE('',#43257,#7433);
#6002=LINE('',#43259,#7434);
#6003=LINE('',#43260,#7435);
#6004=LINE('',#43263,#7436);
#6005=LINE('',#43265,#7437);
#6006=LINE('',#43266,#7438);
#6007=LINE('',#43268,#7439);
#6008=LINE('',#43269,#7440);
#6009=LINE('',#43277,#7441);
#6010=LINE('',#43281,#7442);
#6011=LINE('',#43285,#7443);
#7423=VECTOR('',#26277,1.);
#7424=VECTOR('',#26278,1.);
#7425=VECTOR('',#26279,1.);
#7426=VECTOR('',#26280,1.);
#7427=VECTOR('',#26283,1.);
#7428=VECTOR('',#26284,1.);
#7429=VECTOR('',#26285,1.);
#7430=VECTOR('',#26288,1.);
#7431=VECTOR('',#26289,1.);
#7432=VECTOR('',#26290,1.);
#7433=VECTOR('',#26293,1.);
#7434=VECTOR('',#26294,1.);
#7435=VECTOR('',#26295,1.);
#7436=VECTOR('',#26298,1.);
#7437=VECTOR('',#26299,1.);
#7438=VECTOR('',#26300,1.);
#7439=VECTOR('',#26303,1.);
#7440=VECTOR('',#26304,1.);
#7441=VECTOR('',#26315,0.235);
#7442=VECTOR('',#26320,0.25);
#7443=VECTOR('',#26325,0.2125);
#8120=CIRCLE('',#21139,0.22);
#8121=CIRCLE('',#21141,0.24505);
#8122=CIRCLE('',#21143,0.24505);
#8123=CIRCLE('',#21145,0.175);
#9733=VERTEX_POINT('',#43235);
#9734=VERTEX_POINT('',#43236);
#9735=VERTEX_POINT('',#43238);
#9736=VERTEX_POINT('',#43240);
#9737=VERTEX_POINT('',#43244);
#9738=VERTEX_POINT('',#43246);
#9739=VERTEX_POINT('',#43250);
#9740=VERTEX_POINT('',#43252);
#9741=VERTEX_POINT('',#43256);
#9742=VERTEX_POINT('',#43258);
#9743=VERTEX_POINT('',#43262);
#9744=VERTEX_POINT('',#43264);
#9745=VERTEX_POINT('',#43272);
#9746=VERTEX_POINT('',#43275);
#9747=VERTEX_POINT('',#43279);
#9748=VERTEX_POINT('',#43283);
#12154=EDGE_CURVE('',#9733,#9734,#5991,.T.);
#12155=EDGE_CURVE('',#9733,#9735,#5992,.T.);
#12156=EDGE_CURVE('',#9735,#9736,#5993,.T.);
#12157=EDGE_CURVE('',#9734,#9736,#5994,.T.);
#12158=EDGE_CURVE('',#9737,#9733,#5995,.T.);
#12159=EDGE_CURVE('',#9737,#9738,#5996,.T.);
#12160=EDGE_CURVE('',#9738,#9735,#5997,.T.);
#12161=EDGE_CURVE('',#9739,#9737,#5998,.T.);
#12162=EDGE_CURVE('',#9739,#9740,#5999,.T.);
#12163=EDGE_CURVE('',#9740,#9738,#6000,.T.);
#12164=EDGE_CURVE('',#9741,#9739,#6001,.T.);
#12165=EDGE_CURVE('',#9741,#9742,#6002,.T.);
#12166=EDGE_CURVE('',#9742,#9740,#6003,.T.);
#12167=EDGE_CURVE('',#9743,#9741,#6004,.T.);
#12168=EDGE_CURVE('',#9743,#9744,#6005,.T.);
#12169=EDGE_CURVE('',#9744,#9742,#6006,.T.);
#12170=EDGE_CURVE('',#9734,#9743,#6007,.T.);
#12171=EDGE_CURVE('',#9736,#9744,#6008,.T.);
#12172=EDGE_CURVE('',#9745,#9745,#8120,.T.);
#12173=EDGE_CURVE('',#9746,#9746,#8121,.T.);
#12174=EDGE_CURVE('',#9746,#9745,#6009,.T.);
#12175=EDGE_CURVE('',#9747,#9747,#8122,.F.);
#12176=EDGE_CURVE('',#9747,#9746,#6010,.T.);
#12177=EDGE_CURVE('',#9748,#9748,#8123,.T.);
#12178=EDGE_CURVE('',#9748,#9747,#6011,.T.);
#16979=ORIENTED_EDGE('',*,*,#12154,.F.);
#16980=ORIENTED_EDGE('',*,*,#12155,.T.);
#16981=ORIENTED_EDGE('',*,*,#12156,.T.);
#16982=ORIENTED_EDGE('',*,*,#12157,.F.);
#16983=ORIENTED_EDGE('',*,*,#12158,.F.);
#16984=ORIENTED_EDGE('',*,*,#12159,.T.);
#16985=ORIENTED_EDGE('',*,*,#12160,.T.);
#16986=ORIENTED_EDGE('',*,*,#12155,.F.);
#16987=ORIENTED_EDGE('',*,*,#12161,.F.);
#16988=ORIENTED_EDGE('',*,*,#12162,.T.);
#16989=ORIENTED_EDGE('',*,*,#12163,.T.);
#16990=ORIENTED_EDGE('',*,*,#12159,.F.);
#16991=ORIENTED_EDGE('',*,*,#12164,.F.);
#16992=ORIENTED_EDGE('',*,*,#12165,.T.);
#16993=ORIENTED_EDGE('',*,*,#12166,.T.);
#16994=ORIENTED_EDGE('',*,*,#12162,.F.);
#16995=ORIENTED_EDGE('',*,*,#12167,.F.);
#16996=ORIENTED_EDGE('',*,*,#12168,.T.);
#16997=ORIENTED_EDGE('',*,*,#12169,.T.);
#16998=ORIENTED_EDGE('',*,*,#12165,.F.);
#16999=ORIENTED_EDGE('',*,*,#12170,.F.);
#17000=ORIENTED_EDGE('',*,*,#12157,.T.);
#17001=ORIENTED_EDGE('',*,*,#12171,.T.);
#17002=ORIENTED_EDGE('',*,*,#12168,.F.);
#17003=ORIENTED_EDGE('',*,*,#12171,.F.);
#17004=ORIENTED_EDGE('',*,*,#12156,.F.);
#17005=ORIENTED_EDGE('',*,*,#12160,.F.);
#17006=ORIENTED_EDGE('',*,*,#12163,.F.);
#17007=ORIENTED_EDGE('',*,*,#12166,.F.);
#17008=ORIENTED_EDGE('',*,*,#12169,.F.);
#17009=ORIENTED_EDGE('',*,*,#12172,.F.);
#17010=ORIENTED_EDGE('',*,*,#12154,.T.);
#17011=ORIENTED_EDGE('',*,*,#12170,.T.);
#17012=ORIENTED_EDGE('',*,*,#12167,.T.);
#17013=ORIENTED_EDGE('',*,*,#12164,.T.);
#17014=ORIENTED_EDGE('',*,*,#12161,.T.);
#17015=ORIENTED_EDGE('',*,*,#12158,.T.);
#17016=ORIENTED_EDGE('',*,*,#12173,.F.);
#17017=ORIENTED_EDGE('',*,*,#12174,.T.);
#17018=ORIENTED_EDGE('',*,*,#12172,.T.);
#17019=ORIENTED_EDGE('',*,*,#12174,.F.);
#17020=ORIENTED_EDGE('',*,*,#12175,.F.);
#17021=ORIENTED_EDGE('',*,*,#12176,.T.);
#17022=ORIENTED_EDGE('',*,*,#12173,.T.);
#17023=ORIENTED_EDGE('',*,*,#12176,.F.);
#17024=ORIENTED_EDGE('',*,*,#12177,.F.);
#17025=ORIENTED_EDGE('',*,*,#12178,.T.);
#17026=ORIENTED_EDGE('',*,*,#12175,.T.);
#17027=ORIENTED_EDGE('',*,*,#12178,.F.);
#17028=ORIENTED_EDGE('',*,*,#12177,.T.);
#17489=CYLINDRICAL_SURFACE('',#21142,0.24505);
#18508=ADVANCED_FACE('',(#3184),#2148,.F.);
#18509=ADVANCED_FACE('',(#3185),#2149,.F.);
#18510=ADVANCED_FACE('',(#3186),#2150,.F.);
#18511=ADVANCED_FACE('',(#3187),#2151,.F.);
#18512=ADVANCED_FACE('',(#3188),#2152,.F.);
#18513=ADVANCED_FACE('',(#3189),#2153,.F.);
#18514=ADVANCED_FACE('',(#3190),#2154,.F.);
#18515=ADVANCED_FACE('',(#3191,#1585),#2155,.T.);
#18516=ADVANCED_FACE('',(#3192),#978,.T.);
#18517=ADVANCED_FACE('',(#3193),#17489,.T.);
#18518=ADVANCED_FACE('',(#3194),#979,.T.);
#18519=ADVANCED_FACE('',(#3195),#2156,.T.);
#18619=CLOSED_SHELL('',(#18508,#18509,#18510,#18511,#18512,#18513,#18514,
#18515,#18516,#18517,#18518,#18519));
#21130=AXIS2_PLACEMENT_3D('',#43233,#26273,#26274);
#21131=AXIS2_PLACEMENT_3D('',#43234,#26275,#26276);
#21132=AXIS2_PLACEMENT_3D('',#43243,#26281,#26282);
#21133=AXIS2_PLACEMENT_3D('',#43249,#26286,#26287);
#21134=AXIS2_PLACEMENT_3D('',#43255,#26291,#26292);
#21135=AXIS2_PLACEMENT_3D('',#43261,#26296,#26297);
#21136=AXIS2_PLACEMENT_3D('',#43267,#26301,#26302);
#21137=AXIS2_PLACEMENT_3D('',#43270,#26305,#26306);
#21138=AXIS2_PLACEMENT_3D('',#43271,#26307,#26308);
#21139=AXIS2_PLACEMENT_3D('',#43273,#26309,#26310);
#21140=AXIS2_PLACEMENT_3D('',#43274,#26311,#26312);
#21141=AXIS2_PLACEMENT_3D('',#43276,#26313,#26314);
#21142=AXIS2_PLACEMENT_3D('',#43278,#26316,#26317);
#21143=AXIS2_PLACEMENT_3D('',#43280,#26318,#26319);
#21144=AXIS2_PLACEMENT_3D('',#43282,#26321,#26322);
#21145=AXIS2_PLACEMENT_3D('',#43284,#26323,#26324);
#21146=AXIS2_PLACEMENT_3D('',#43286,#26326,#26327);
#26273=DIRECTION('axis',(0.,0.,1.));
#26274=DIRECTION('refdir',(1.,0.,0.));
#26275=DIRECTION('center_axis',(0.866025403784439,0.,-0.5));
#26276=DIRECTION('ref_axis',(0.5,0.,0.866025403784439));
#26277=DIRECTION('',(0.5,0.,0.866025403784439));
#26278=DIRECTION('',(0.,-1.,0.));
#26279=DIRECTION('',(0.5,0.,0.866025403784439));
#26280=DIRECTION('',(0.,-1.,0.));
#26281=DIRECTION('center_axis',(1.92296268638356E-16,0.,-1.));
#26282=DIRECTION('ref_axis',(1.,0.,1.92296268638356E-16));
#26283=DIRECTION('',(1.,0.,1.92296268638356E-16));
#26284=DIRECTION('',(0.,-1.,0.));
#26285=DIRECTION('',(1.,0.,1.92296268638356E-16));
#26286=DIRECTION('center_axis',(-0.866025403784439,0.,-0.5));
#26287=DIRECTION('ref_axis',(0.5,0.,-0.866025403784439));
#26288=DIRECTION('',(0.5,0.,-0.866025403784439));
#26289=DIRECTION('',(0.,-1.,0.));
#26290=DIRECTION('',(0.5,0.,-0.866025403784438));
#26291=DIRECTION('center_axis',(-0.866025403784439,0.,0.5));
#26292=DIRECTION('ref_axis',(-0.5,0.,-0.866025403784439));
#26293=DIRECTION('',(-0.5,0.,-0.866025403784439));
#26294=DIRECTION('',(0.,-1.,0.));
#26295=DIRECTION('',(-0.5,0.,-0.866025403784439));
#26296=DIRECTION('center_axis',(-1.92296268638356E-16,0.,1.));
#26297=DIRECTION('ref_axis',(-1.,0.,-1.92296268638356E-16));
#26298=DIRECTION('',(-1.,0.,-1.92296268638356E-16));
#26299=DIRECTION('',(0.,-1.,0.));
#26300=DIRECTION('',(-1.,0.,-1.92296268638356E-16));
#26301=DIRECTION('center_axis',(0.866025403784439,0.,0.5));
#26302=DIRECTION('ref_axis',(-0.5,0.,0.866025403784439));
#26303=DIRECTION('',(-0.5,0.,0.866025403784439));
#26304=DIRECTION('',(-0.5,0.,0.866025403784439));
#26305=DIRECTION('center_axis',(0.,-1.,0.));
#26306=DIRECTION('ref_axis',(0.,0.,-1.));
#26307=DIRECTION('center_axis',(0.,1.,0.));
#26308=DIRECTION('ref_axis',(0.,0.,1.));
#26309=DIRECTION('center_axis',(0.,-1.,0.));
#26310=DIRECTION('ref_axis',(1.,0.,0.));
#26311=DIRECTION('center_axis',(0.,-1.,0.));
#26312=DIRECTION('ref_axis',(1.,0.,0.));
#26313=DIRECTION('center_axis',(0.,-1.,0.));
#26314=DIRECTION('ref_axis',(1.,0.,0.));
#26315=DIRECTION('',(0.707106781186547,0.707106781186548,8.65956056235493E-17));
#26316=DIRECTION('center_axis',(0.,-1.,0.));
#26317=DIRECTION('ref_axis',(1.,0.,0.));
#26318=DIRECTION('center_axis',(0.,1.,0.));
#26319=DIRECTION('ref_axis',(1.,0.,0.));
#26320=DIRECTION('',(0.,1.,0.));
#26321=DIRECTION('center_axis',(0.,1.,0.));
#26322=DIRECTION('ref_axis',(1.,0.,0.));
#26323=DIRECTION('center_axis',(0.,-1.,0.));
#26324=DIRECTION('ref_axis',(1.,0.,0.));
#26325=DIRECTION('',(-0.707106781186547,0.707106781186548,-8.65956056235493E-17));
#26326=DIRECTION('center_axis',(0.,-1.,0.));
#26327=DIRECTION('ref_axis',(0.,0.,-1.));
#43233=CARTESIAN_POINT('',(0.,0.,0.));
#43234=CARTESIAN_POINT('Origin',(0.0721687836487032,0.,-0.125));
#43235=CARTESIAN_POINT('',(0.0721687836487032,0.,-0.125));
#43236=CARTESIAN_POINT('',(0.144337567297406,0.,0.));
#43237=CARTESIAN_POINT('',(0.117710979560879,0.,-0.0461186027918559));
#43238=CARTESIAN_POINT('',(0.0721687836487032,-0.25,-0.125));
#43239=CARTESIAN_POINT('',(0.0721687836487032,0.,-0.125));
#43240=CARTESIAN_POINT('',(0.144337567297406,-0.25,0.));
#43241=CARTESIAN_POINT('',(0.144337567297406,-0.25,0.));
#43242=CARTESIAN_POINT('',(0.144337567297406,0.,0.));
#43243=CARTESIAN_POINT('Origin',(-0.0721687836487032,0.,-0.125));
#43244=CARTESIAN_POINT('',(-0.0721687836487032,0.,-0.125));
#43245=CARTESIAN_POINT('',(0.0739156081756484,0.,-0.125));
#43246=CARTESIAN_POINT('',(-0.0721687836487032,-0.25,-0.125));
#43247=CARTESIAN_POINT('',(-0.0721687836487032,0.,-0.125));
#43248=CARTESIAN_POINT('',(0.0721687836487032,-0.25,-0.125));
#43249=CARTESIAN_POINT('Origin',(-0.144337567297406,0.,-4.16333634234434E-17));
#43250=CARTESIAN_POINT('',(-0.144337567297406,0.,-1.76762539787485E-17));
#43251=CARTESIAN_POINT('',(-0.0987953713852306,0.,-0.0788813972081442));
#43252=CARTESIAN_POINT('',(-0.144337567297406,-0.25,-2.77555756156289E-17));
#43253=CARTESIAN_POINT('',(-0.144337567297406,0.,-1.76762539787485E-17));
#43254=CARTESIAN_POINT('',(-0.0721687836487032,-0.25,-0.125));
#43255=CARTESIAN_POINT('Origin',(-0.0721687836487033,0.,0.125));
#43256=CARTESIAN_POINT('',(-0.0721687836487033,0.,0.125));
#43257=CARTESIAN_POINT('',(-0.0627109795608791,0.,0.141381397208144));
#43258=CARTESIAN_POINT('',(-0.0721687836487033,-0.25,0.125));
#43259=CARTESIAN_POINT('',(-0.0721687836487033,0.,0.125));
#43260=CARTESIAN_POINT('',(-0.144337567297406,-0.25,-1.76762539787485E-17));
#43261=CARTESIAN_POINT('Origin',(0.0721687836487032,0.,0.125));
#43262=CARTESIAN_POINT('',(0.0721687836487032,0.,0.125));
#43263=CARTESIAN_POINT('',(0.146084391824352,0.,0.125));
#43264=CARTESIAN_POINT('',(0.0721687836487032,-0.25,0.125));
#43265=CARTESIAN_POINT('',(0.0721687836487032,0.,0.125));
#43266=CARTESIAN_POINT('',(-0.0721687836487033,-0.25,0.125));
#43267=CARTESIAN_POINT('Origin',(0.144337567297406,0.,0.));
#43268=CARTESIAN_POINT('',(0.153795371385231,0.,-0.0163813972081441));
#43269=CARTESIAN_POINT('',(0.0721687836487032,-0.25,0.125));
#43270=CARTESIAN_POINT('Origin',(0.,-0.25,0.));
#43271=CARTESIAN_POINT('Origin',(0.22,0.,0.));
#43272=CARTESIAN_POINT('',(-0.22,-8.67361737988404E-18,-2.69422295812418E-17));
#43273=CARTESIAN_POINT('Origin',(0.,0.,0.));
#43274=CARTESIAN_POINT('Origin',(0.,-0.015,0.));
#43275=CARTESIAN_POINT('',(-0.24505,-0.02505,-3.00099698131059E-17));
#43276=CARTESIAN_POINT('Origin',(0.,-0.02505,0.));
#43277=CARTESIAN_POINT('',(-0.235,-0.015,-2.87791997799628E-17));
#43278=CARTESIAN_POINT('Origin',(0.,-0.3775,0.));
#43279=CARTESIAN_POINT('',(-0.24505,-0.72995,3.00099698131059E-17));
#43280=CARTESIAN_POINT('Origin',(0.,-0.72995,0.));
#43281=CARTESIAN_POINT('',(-0.24505,-0.3775,-3.00099698131059E-17));
#43282=CARTESIAN_POINT('Origin',(0.,-0.7625,0.));
#43283=CARTESIAN_POINT('',(-0.175,-0.8,-2.14313189850787E-17));
#43284=CARTESIAN_POINT('Origin',(0.,-0.8,0.));
#43285=CARTESIAN_POINT('',(-0.2125,-0.7625,-2.60237444818813E-17));
#43286=CARTESIAN_POINT('Origin',(0.,-0.8,0.));
#43450=UNCERTAINTY_MEASURE_WITH_UNIT(LENGTH_MEASURE(0.001),#43522,
'DISTANCE_ACCURACY_VALUE',
'Maximum model space distance between geometric entities at asserted c
onnectivities');
#43453=UNCERTAINTY_MEASURE_WITH_UNIT(LENGTH_MEASURE(0.001),#43522,
'DISTANCE_ACCURACY_VALUE',
'Maximum model space distance between geometric entities at asserted c
onnectivities');
#43518=(
GEOMETRIC_REPRESENTATION_CONTEXT(3)
GLOBAL_UNCERTAINTY_ASSIGNED_CONTEXT((#43450))
GLOBAL_UNIT_ASSIGNED_CONTEXT((#43522,#43524,#43525))
REPRESENTATION_CONTEXT('','3D')
);
#43521=(
GEOMETRIC_REPRESENTATION_CONTEXT(3)
GLOBAL_UNCERTAINTY_ASSIGNED_CONTEXT((#43453))
GLOBAL_UNIT_ASSIGNED_CONTEXT((#43522,#43524,#43525))
REPRESENTATION_CONTEXT('','3D')
);
#43522=(
LENGTH_UNIT()
NAMED_UNIT(*)
SI_UNIT(.CENTI.,.METRE.)
);
#43524=(
NAMED_UNIT(*)
PLANE_ANGLE_UNIT()
SI_UNIT($,.RADIAN.)
);
#43525=(
NAMED_UNIT(*)
SI_UNIT($,.STERADIAN.)
SOLID_ANGLE_UNIT()
);
#43590=SHAPE_DEFINITION_REPRESENTATION(#43777,#43858);
#43777=PRODUCT_DEFINITION_SHAPE('',$,#43926);
#43858=SHAPE_REPRESENTATION('',(#21130),#43518);
#43861=PRODUCT_DEFINITION_CONTEXT('part definition',#44064,'design');
#43926=PRODUCT_DEFINITION('Socket Set Screw - M5x8',
'Socket Set Screw - M5x8',#43993,#43861);
#43993=PRODUCT_DEFINITION_FORMATION('',$,#44130);
#44064=APPLICATION_CONTEXT(
'Core Data for Automotive Mechanical Design Process');
#44065=PRODUCT_CONTEXT('part definition',#44064,'mechanical');
#44130=PRODUCT('Socket Set Screw - M5x8','Socket Set Screw - M5x8',
'Socket Set Screw - M5x8',(#44065));
#44203=COLOUR_RGB('Black',0.12,0.14,0.17);
#44204=FILL_AREA_STYLE_COLOUR('',#44203);
#44205=FILL_AREA_STYLE('',(#44204));
#44206=SURFACE_STYLE_FILL_AREA(#44205);
#44207=SURFACE_SIDE_STYLE('',(#44206));
#44208=SURFACE_STYLE_USAGE(.BOTH.,#44207);
#44209=PRESENTATION_STYLE_ASSIGNMENT((#44208));
ENDSEC;
END-ISO-10303-21;
